ISO-10303-21;
HEADER;
/* Generated by software containing ST-Developer
 * from STEP Tools, Inc. (www.steptools.com) 
 */

FILE_DESCRIPTION(
/* description */ ('Hinged panel with latch'),
/* implementation_level */ '2;1');

FILE_NAME(
/* name */ 'Cap Screw - M4x16.step',
/* time_stamp */ '2026-10-27T20:36:01-07:00',
/* author */ (''),
/* organization */ (''),
/* preprocessor_version */ 'ST-DEVELOPER v20.2',
/* originating_system */ 'Autodesk Translation Framework v15.17.0.0',
/* authorisation */ '');

FILE_SCHEMA (('AUTOMOTIVE_DESIGN { 1 0 10303 214 3 1 1 }'));
ENDSEC;

DATA;
#10=MECHANICAL_DESIGN_GEOMETRIC_PRESENTATION_REPRESENTATION('',(#306),#6743);
#232=ORIENTED_CLOSED_SHELL('',*,#3810,.F.);
#235=BREP_WITH_VOIDS('Body1',#3809,(#232));
#245=CONICAL_SURFACE('',#4212,0.325,0.785398163397448);
#246=CONICAL_SURFACE('',#4216,0.335,0.785398163397448);
#247=CONICAL_SURFACE('',#4220,0.21,0.463647609000806);
#248=CONICAL_SURFACE('',#4224,0.18,0.785398163397448);
#274=SHAPE_REPRESENTATION_RELATIONSHIP('SRR','None',#6850,#290);
#290=ADVANCED_BREP_SHAPE_REPRESENTATION('',(#235),#6736);
#306=STYLED_ITEM('',(#7010),#235);
#362=FACE_BOUND('',#909,.T.);
#477=PLANE('',#4210);
#478=PLANE('',#4218);
#479=PLANE('',#4226);
#480=PLANE('',#4227);
#481=PLANE('',#4228);
#482=PLANE('',#4229);
#483=PLANE('',#4230);
#484=PLANE('',#4231);
#485=PLANE('',#4232);
#486=PLANE('',#4233);
#487=PLANE('',#4234);
#661=FACE_OUTER_BOUND('',#904,.T.);
#662=FACE_OUTER_BOUND('',#905,.T.);
#663=FACE_OUTER_BOUND('',#906,.T.);
#664=FACE_OUTER_BOUND('',#907,.T.);
#665=FACE_OUTER_BOUND('',#908,.T.);
#666=FACE_OUTER_BOUND('',#910,.T.);
#667=FACE_OUTER_BOUND('',#911,.T.);
#668=FACE_OUTER_BOUND('',#912,.T.);
#669=FACE_OUTER_BOUND('',#913,.T.);
#670=FACE_OUTER_BOUND('',#914,.T.);
#671=FACE_OUTER_BOUND('',#915,.T.);
#672=FACE_OUTER_BOUND('',#916,.T.);
#673=FACE_OUTER_BOUND('',#917,.T.);
#674=FACE_OUTER_BOUND('',#918,.T.);
#675=FACE_OUTER_BOUND('',#919,.T.);
#676=FACE_OUTER_BOUND('',#920,.T.);
#677=FACE_OUTER_BOUND('',#921,.T.);
#904=EDGE_LOOP('',(#3282));
#905=EDGE_LOOP('',(#3283,#3284,#3285,#3286));
#906=EDGE_LOOP('',(#3287,#3288,#3289,#3290));
#907=EDGE_LOOP('',(#3291,#3292,#3293,#3294));
#908=EDGE_LOOP('',(#3295));
#909=EDGE_LOOP('',(#3296));
#910=EDGE_LOOP('',(#3297,#3298,#3299,#3300));
#911=EDGE_LOOP('',(#3301,#3302,#3303,#3304));
#912=EDGE_LOOP('',(#3305,#3306,#3307,#3308));
#913=EDGE_LOOP('',(#3309));
#914=EDGE_LOOP('',(#3310,#3311,#3312,#3313));
#915=EDGE_LOOP('',(#3314,#3315,#3316,#3317));
#916=EDGE_LOOP('',(#3318,#3319,#3320,#3321));
#917=EDGE_LOOP('',(#3322,#3323,#3324,#3325));
#918=EDGE_LOOP('',(#3326,#3327,#3328,#3329));
#919=EDGE_LOOP('',(#3330,#3331,#3332,#3333));
#920=EDGE_LOOP('',(#3334,#3335,#3336,#3337,#3338,#3339));
#921=EDGE_LOOP('',(#3340,#3341,#3342,#3343,#3344,#3345));
#1258=LINE('',#6313,#1616);
#1259=LINE('',#6317,#1617);
#1260=LINE('',#6321,#1618);
#1261=LINE('',#6328,#1619);
#1262=LINE('',#6332,#1620);
#1263=LINE('',#6336,#1621);
#1264=LINE('',#6341,#1622);
#1265=LINE('',#6343,#1623);
#1266=LINE('',#6345,#1624);
#1267=LINE('',#6346,#1625);
#1268=LINE('',#6349,#1626);
#1269=LINE('',#6351,#1627);
#1270=LINE('',#6352,#1628);
#1271=LINE('',#6355,#1629);
#1272=LINE('',#6357,#1630);
#1273=LINE('',#6358,#1631);
#1274=LINE('',#6361,#1632);
#1275=LINE('',#6363,#1633);
#1276=LINE('',#6364,#1634);
#1277=LINE('',#6367,#1635);
#1278=LINE('',#6369,#1636);
#1279=LINE('',#6370,#1637);
#1280=LINE('',#6372,#1638);
#1281=LINE('',#6373,#1639);
#1616=VECTOR('',#5080,0.325);
#1617=VECTOR('',#5085,0.35);
#1618=VECTOR('',#5090,0.335);
#1619=VECTOR('',#5099,0.21);
#1620=VECTOR('',#5104,0.2);
#1621=VECTOR('',#5109,0.18);
#1622=VECTOR('',#5114,1.);
#1623=VECTOR('',#5115,1.);
#1624=VECTOR('',#5116,1.);
#1625=VECTOR('',#5117,1.);
#1626=VECTOR('',#5120,1.);
#1627=VECTOR('',#5121,1.);
#1628=VECTOR('',#5122,1.);
#1629=VECTOR('',#5125,1.);
#1630=VECTOR('',#5126,1.);
#1631=VECTOR('',#5127,1.);
#1632=VECTOR('',#5130,1.);
#1633=VECTOR('',#5131,1.);
#1634=VECTOR('',#5132,1.);
#1635=VECTOR('',#5135,1.);
#1636=VECTOR('',#5136,1.);
#1637=VECTOR('',#5137,1.);
#1638=VECTOR('',#5140,1.);
#1639=VECTOR('',#5141,1.);
#1760=CIRCLE('',#4211,0.3);
#1761=CIRCLE('',#4213,0.35);
#1762=CIRCLE('',#4215,0.35);
#1763=CIRCLE('',#4217,0.32);
#1764=CIRCLE('',#4219,0.22);
#1765=CIRCLE('',#4221,0.1954);
#1766=CIRCLE('',#4223,0.1954);
#1767=CIRCLE('',#4225,0.16);
#2020=VERTEX_POINT('',#6308);
#2021=VERTEX_POINT('',#6311);
#2022=VERTEX_POINT('',#6315);
#2023=VERTEX_POINT('',#6319);
#2024=VERTEX_POINT('',#6323);
#2025=VERTEX_POINT('',#6326);
#2026=VERTEX_POINT('',#6330);
#2027=VERTEX_POINT('',#6334);
#2028=VERTEX_POINT('',#6339);
#2029=VERTEX_POINT('',#6340);
#2030=VERTEX_POINT('',#6342);
#2031=VERTEX_POINT('',#6344);
#2032=VERTEX_POINT('',#6348);
#2033=VERTEX_POINT('',#6350);
#2034=VERTEX_POINT('',#6354);
#2035=VERTEX_POINT('',#6356);
#2036=VERTEX_POINT('',#6360);
#2037=VERTEX_POINT('',#6362);
#2038=VERTEX_POINT('',#6366);
#2039=VERTEX_POINT('',#6368);
#2453=EDGE_CURVE('',#2020,#2020,#1760,.T.);
#2454=EDGE_CURVE('',#2021,#2021,#1761,.T.);
#2455=EDGE_CURVE('',#2021,#2020,#1258,.T.);
#2456=EDGE_CURVE('',#2022,#2022,#1762,.T.);
#2457=EDGE_CURVE('',#2022,#2021,#1259,.T.);
#2458=EDGE_CURVE('',#2023,#2023,#1763,.T.);
#2459=EDGE_CURVE('',#2023,#2022,#1260,.T.);
#2460=EDGE_CURVE('',#2024,#2024,#1764,.T.);
#2461=EDGE_CURVE('',#2025,#2025,#1765,.F.);
#2462=EDGE_CURVE('',#2025,#2024,#1261,.T.);
#2463=EDGE_CURVE('',#2026,#2026,#1766,.F.);
#2464=EDGE_CURVE('',#2026,#2025,#1262,.T.);
#2465=EDGE_CURVE('',#2027,#2027,#1767,.T.);
#2466=EDGE_CURVE('',#2027,#2026,#1263,.T.);
#2467=EDGE_CURVE('',#2028,#2029,#1264,.T.);
#2468=EDGE_CURVE('',#2029,#2030,#1265,.T.);
#2469=EDGE_CURVE('',#2030,#2031,#1266,.T.);
#2470=EDGE_CURVE('',#2028,#2031,#1267,.T.);
#2471=EDGE_CURVE('',#2029,#2032,#1268,.T.);
#2472=EDGE_CURVE('',#2032,#2033,#1269,.T.);
#2473=EDGE_CURVE('',#2033,#2030,#1270,.T.);
#2474=EDGE_CURVE('',#2032,#2034,#1271,.T.);
#2475=EDGE_CURVE('',#2034,#2035,#1272,.T.);
#2476=EDGE_CURVE('',#2035,#2033,#1273,.T.);
#2477=EDGE_CURVE('',#2034,#2036,#1274,.T.);
#2478=EDGE_CURVE('',#2036,#2037,#1275,.T.);
#2479=EDGE_CURVE('',#2037,#2035,#1276,.T.);
#2480=EDGE_CURVE('',#2036,#2038,#1277,.T.);
#2481=EDGE_CURVE('',#2038,#2039,#1278,.T.);
#2482=EDGE_CURVE('',#2039,#2037,#1279,.T.);
#2483=EDGE_CURVE('',#2038,#2028,#1280,.T.);
#2484=EDGE_CURVE('',#2031,#2039,#1281,.T.);
#3282=ORIENTED_EDGE('',*,*,#2453,.F.);
#3283=ORIENTED_EDGE('',*,*,#2454,.F.);
#3284=ORIENTED_EDGE('',*,*,#2455,.T.);
#3285=ORIENTED_EDGE('',*,*,#2453,.T.);
#3286=ORIENTED_EDGE('',*,*,#2455,.F.);
#3287=ORIENTED_EDGE('',*,*,#2456,.F.);
#3288=ORIENTED_EDGE('',*,*,#2457,.T.);
#3289=ORIENTED_EDGE('',*,*,#2454,.T.);
#3290=ORIENTED_EDGE('',*,*,#2457,.F.);
#3291=ORIENTED_EDGE('',*,*,#2458,.F.);
#3292=ORIENTED_EDGE('',*,*,#2459,.T.);
#3293=ORIENTED_EDGE('',*,*,#2456,.T.);
#3294=ORIENTED_EDGE('',*,*,#2459,.F.);
#3295=ORIENTED_EDGE('',*,*,#2458,.T.);
#3296=ORIENTED_EDGE('',*,*,#2460,.F.);
#3297=ORIENTED_EDGE('',*,*,#2461,.F.);
#3298=ORIENTED_EDGE('',*,*,#2462,.T.);
#3299=ORIENTED_EDGE('',*,*,#2460,.T.);
#3300=ORIENTED_EDGE('',*,*,#2462,.F.);
#3301=ORIENTED_EDGE('',*,*,#2463,.F.);
#3302=ORIENTED_EDGE('',*,*,#2464,.T.);
#3303=ORIENTED_EDGE('',*,*,#2461,.T.);
#3304=ORIENTED_EDGE('',*,*,#2464,.F.);
#3305=ORIENTED_EDGE('',*,*,#2465,.F.);
#3306=ORIENTED_EDGE('',*,*,#2466,.T.);
#3307=ORIENTED_EDGE('',*,*,#2463,.T.);
#3308=ORIENTED_EDGE('',*,*,#2466,.F.);
#3309=ORIENTED_EDGE('',*,*,#2465,.T.);
#3310=ORIENTED_EDGE('',*,*,#2467,.T.);
#3311=ORIENTED_EDGE('',*,*,#2468,.T.);
#3312=ORIENTED_EDGE('',*,*,#2469,.T.);
#3313=ORIENTED_EDGE('',*,*,#2470,.F.);
#3314=ORIENTED_EDGE('',*,*,#2471,.T.);
#3315=ORIENTED_EDGE('',*,*,#2472,.T.);
#3316=ORIENTED_EDGE('',*,*,#2473,.T.);
#3317=ORIENTED_EDGE('',*,*,#2468,.F.);
#3318=ORIENTED_EDGE('',*,*,#2474,.T.);
#3319=ORIENTED_EDGE('',*,*,#2475,.T.);
#3320=ORIENTED_EDGE('',*,*,#2476,.T.);
#3321=ORIENTED_EDGE('',*,*,#2472,.F.);
#3322=ORIENTED_EDGE('',*,*,#2477,.T.);
#3323=ORIENTED_EDGE('',*,*,#2478,.T.);
#3324=ORIENTED_EDGE('',*,*,#2479,.T.);
#3325=ORIENTED_EDGE('',*,*,#2475,.F.);
#3326=ORIENTED_EDGE('',*,*,#2480,.T.);
#3327=ORIENTED_EDGE('',*,*,#2481,.T.);
#3328=ORIENTED_EDGE('',*,*,#2482,.T.);
#3329=ORIENTED_EDGE('',*,*,#2478,.F.);
#3330=ORIENTED_EDGE('',*,*,#2483,.T.);
#3331=ORIENTED_EDGE('',*,*,#2470,.T.);
#3332=ORIENTED_EDGE('',*,*,#2484,.T.);
#3333=ORIENTED_EDGE('',*,*,#2481,.F.);
#3334=ORIENTED_EDGE('',*,*,#2483,.F.);
#3335=ORIENTED_EDGE('',*,*,#2480,.F.);
#3336=ORIENTED_EDGE('',*,*,#2477,.F.);
#3337=ORIENTED_EDGE('',*,*,#2474,.F.);
#3338=ORIENTED_EDGE('',*,*,#2471,.F.);
#3339=ORIENTED_EDGE('',*,*,#2467,.F.);
#3340=ORIENTED_EDGE('',*,*,#2484,.F.);
#3341=ORIENTED_EDGE('',*,*,#2469,.F.);
#3342=ORIENTED_EDGE('',*,*,#2473,.F.);
#3343=ORIENTED_EDGE('',*,*,#2476,.F.);
#3344=ORIENTED_EDGE('',*,*,#2479,.F.);
#3345=ORIENTED_EDGE('',*,*,#2482,.F.);
#3583=CYLINDRICAL_SURFACE('',#4214,0.35);
#3584=CYLINDRICAL_SURFACE('',#4222,0.1954);
#3730=ADVANCED_FACE('',(#661),#477,.T.);
#3731=ADVANCED_FACE('',(#662),#245,.T.);
#3732=ADVANCED_FACE('',(#663),#3583,.T.);
#3733=ADVANCED_FACE('',(#664),#246,.T.);
#3734=ADVANCED_FACE('',(#665,#362),#478,.T.);
#3735=ADVANCED_FACE('',(#666),#247,.T.);
#3736=ADVANCED_FACE('',(#667),#3584,.T.);
#3737=ADVANCED_FACE('',(#668),#248,.T.);
#3738=ADVANCED_FACE('',(#669),#479,.T.);
#3739=ADVANCED_FACE('',(#670),#480,.F.);
#3740=ADVANCED_FACE('',(#671),#481,.F.);
#3741=ADVANCED_FACE('',(#672),#482,.F.);
#3742=ADVANCED_FACE('',(#673),#483,.F.);
#3743=ADVANCED_FACE('',(#674),#484,.F.);
#3744=ADVANCED_FACE('',(#675),#485,.F.);
#3745=ADVANCED_FACE('',(#676),#486,.F.);
#3746=ADVANCED_FACE('',(#677),#487,.F.);
#3809=CLOSED_SHELL('',(#3730,#3731,#3732,#3733,#3734,#3735,#3736,#3737,
#3738));
#3810=CLOSED_SHELL('',(#3739,#3740,#3741,#3742,#3743,#3744,#3745,#3746));
#4209=AXIS2_PLACEMENT_3D('',#6306,#5070,#5071);
#4210=AXIS2_PLACEMENT_3D('',#6307,#5072,#5073);
#4211=AXIS2_PLACEMENT_3D('',#6309,#5074,#5075);
#4212=AXIS2_PLACEMENT_3D('',#6310,#5076,#5077);
#4213=AXIS2_PLACEMENT_3D('',#6312,#5078,#5079);
#4214=AXIS2_PLACEMENT_3D('',#6314,#5081,#5082);
#4215=AXIS2_PLACEMENT_3D('',#6316,#5083,#5084);
#4216=AXIS2_PLACEMENT_3D('',#6318,#5086,#5087);
#4217=AXIS2_PLACEMENT_3D('',#6320,#5088,#5089);
#4218=AXIS2_PLACEMENT_3D('',#6322,#5091,#5092);
#4219=AXIS2_PLACEMENT_3D('',#6324,#5093,#5094);
#4220=AXIS2_PLACEMENT_3D('',#6325,#5095,#5096);
#4221=AXIS2_PLACEMENT_3D('',#6327,#5097,#5098);
#4222=AXIS2_PLACEMENT_3D('',#6329,#5100,#5101);
#4223=AXIS2_PLACEMENT_3D('',#6331,#5102,#5103);
#4224=AXIS2_PLACEMENT_3D('',#6333,#5105,#5106);
#4225=AXIS2_PLACEMENT_3D('',#6335,#5107,#5108);
#4226=AXIS2_PLACEMENT_3D('',#6337,#5110,#5111);
#4227=AXIS2_PLACEMENT_3D('',#6338,#5112,#5113);
#4228=AXIS2_PLACEMENT_3D('',#6347,#5118,#5119);
#4229=AXIS2_PLACEMENT_3D('',#6353,#5123,#5124);
#4230=AXIS2_PLACEMENT_3D('',#6359,#5128,#5129);
#4231=AXIS2_PLACEMENT_3D('',#6365,#5133,#5134);
#4232=AXIS2_PLACEMENT_3D('',#6371,#5138,#5139);
#4233=AXIS2_PLACEMENT_3D('',#6374,#5142,#5143);
#4234=AXIS2_PLACEMENT_3D('',#6375,#5144,#5145);
#5070=DIRECTION('axis',(0.,0.,1.));
#5071=DIRECTION('refdir',(1.,0.,0.));
#5072=DIRECTION('center_axis',(0.,1.,0.));
#5073=DIRECTION('ref_axis',(0.,0.,1.));
#5074=DIRECTION('center_axis',(0.,-1.,0.));
#5075=DIRECTION('ref_axis',(1.,0.,0.));
#5076=DIRECTION('center_axis',(0.,-1.,0.));
#5077=DIRECTION('ref_axis',(1.,0.,0.));
#5078=DIRECTION('center_axis',(0.,-1.,0.));
#5079=DIRECTION('ref_axis',(1.,0.,0.));
#5080=DIRECTION('',(0.707106781186547,0.707106781186548,8.65956056235493E-17));
#5081=DIRECTION('center_axis',(0.,-1.,0.));
#5082=DIRECTION('ref_axis',(1.,0.,0.));
#5083=DIRECTION('center_axis',(0.,-1.,0.));
#5084=DIRECTION('ref_axis',(1.,0.,0.));
#5085=DIRECTION('',(0.,1.,0.));
#5086=DIRECTION('center_axis',(0.,1.,0.));
#5087=DIRECTION('ref_axis',(1.,0.,0.));
#5088=DIRECTION('center_axis',(0.,-1.,0.));
#5089=DIRECTION('ref_axis',(1.,0.,0.));
#5090=DIRECTION('',(-0.707106781186547,0.707106781186548,-8.65956056235493E-17));
#5091=DIRECTION('center_axis',(0.,-1.,0.));
#5092=DIRECTION('ref_axis',(0.,0.,-1.));
#5093=DIRECTION('center_axis',(0.,-1.,0.));
#5094=DIRECTION('ref_axis',(1.,0.,0.));
#5095=DIRECTION('center_axis',(0.,1.,0.));
#5096=DIRECTION('ref_axis',(1.,0.,0.));
#5097=DIRECTION('center_axis',(0.,1.,0.));
#5098=DIRECTION('ref_axis',(1.,0.,0.));
#5099=DIRECTION('',(-0.447213595499958,0.894427190999916,-5.47678698264203E-17));
#5100=DIRECTION('center_axis',(0.,-1.,0.));
#5101=DIRECTION('ref_axis',(1.,0.,0.));
#5102=DIRECTION('center_axis',(0.,1.,0.));
#5103=DIRECTION('ref_axis',(1.,0.,0.));
#5104=DIRECTION('',(0.,1.,0.));
#5105=DIRECTION('center_axis',(0.,1.,0.));
#5106=DIRECTION('ref_axis',(1.,0.,0.));
#5107=DIRECTION('center_axis',(0.,-1.,0.));
#5108=DIRECTION('ref_axis',(1.,0.,0.));
#5109=DIRECTION('',(-0.707106781186547,0.707106781186548,-8.65956056235493E-17));
#5110=DIRECTION('center_axis',(0.,-1.,0.));
#5111=DIRECTION('ref_axis',(0.,0.,-1.));
#5112=DIRECTION('center_axis',(0.866025403784439,0.,-0.5));
#5113=DIRECTION('ref_axis',(0.5,0.,0.866025403784439));
#5114=DIRECTION('',(-0.5,0.,-0.866025403784439));
#5115=DIRECTION('',(0.,-1.,0.));
#5116=DIRECTION('',(0.5,0.,0.866025403784439));
#5117=DIRECTION('',(0.,-1.,0.));
#5118=DIRECTION('center_axis',(1.60246890531964E-16,0.,-1.));
#5119=DIRECTION('ref_axis',(1.,0.,1.60246890531964E-16));
#5120=DIRECTION('',(-1.,0.,-1.60246890531964E-16));
#5121=DIRECTION('',(0.,-1.,0.));
#5122=DIRECTION('',(1.,0.,1.60246890531964E-16));
#5123=DIRECTION('center_axis',(-0.866025403784439,0.,-0.5));
#5124=DIRECTION('ref_axis',(0.5,0.,-0.866025403784439));
#5125=DIRECTION('',(-0.5,0.,0.866025403784439));
#5126=DIRECTION('',(0.,-1.,0.));
#5127=DIRECTION('',(0.5,0.,-0.866025403784439));
#5128=DIRECTION('center_axis',(-0.866025403784439,0.,0.5));
#5129=DIRECTION('ref_axis',(-0.5,0.,-0.866025403784439));
#5130=DIRECTION('',(0.5,0.,0.866025403784439));
#5131=DIRECTION('',(0.,-1.,0.));
#5132=DIRECTION('',(-0.5,0.,-0.866025403784439));
#5133=DIRECTION('center_axis',(-1.60246890531964E-16,0.,1.));
#5134=DIRECTION('ref_axis',(-1.,0.,-1.60246890531964E-16));
#5135=DIRECTION('',(1.,0.,1.60246890531964E-16));
#5136=DIRECTION('',(0.,-1.,0.));
#5137=DIRECTION('',(-1.,0.,-1.60246890531964E-16));
#5138=DIRECTION('center_axis',(0.866025403784439,0.,0.5));
#5139=DIRECTION('ref_axis',(-0.5,0.,0.866025403784439));
#5140=DIRECTION('',(0.5,0.,-0.866025403784439));
#5141=DIRECTION('',(-0.5,0.,0.866025403784439));
#5142=DIRECTION('center_axis',(0.,1.,0.));
#5143=DIRECTION('ref_axis',(1.,0.,0.));
#5144=DIRECTION('center_axis',(0.,-1.,0.));
#5145=DIRECTION('ref_axis',(0.,0.,-1.));
#6306=CARTESIAN_POINT('',(0.,0.,0.));
#6307=CARTESIAN_POINT('Origin',(0.3,0.4,0.));
#6308=CARTESIAN_POINT('',(-0.3,0.4,-3.67394039744206E-17));
#6309=CARTESIAN_POINT('Origin',(0.,0.4,0.));
#6310=CARTESIAN_POINT('Origin',(0.,0.375,0.));
#6311=CARTESIAN_POINT('',(-0.35,0.35,-4.28626379701573E-17));
#6312=CARTESIAN_POINT('Origin',(0.,0.35,0.));
#6313=CARTESIAN_POINT('',(-0.325,0.375,-3.9801020972289E-17));
#6314=CARTESIAN_POINT('Origin',(0.,0.19,0.));
#6315=CARTESIAN_POINT('',(-0.35,0.03,-4.28626379701574E-17));
#6316=CARTESIAN_POINT('Origin',(0.,0.03,0.));
#6317=CARTESIAN_POINT('',(-0.35,0.19,-4.28626379701574E-17));
#6318=CARTESIAN_POINT('Origin',(0.,0.0149999999999999,0.));
#6319=CARTESIAN_POINT('',(-0.32,-3.29597460435593E-17,-3.91886975727153E-17));
#6320=CARTESIAN_POINT('Origin',(0.,0.,0.));
#6321=CARTESIAN_POINT('',(-0.335,0.0149999999999999,-4.10256677714363E-17));
#6322=CARTESIAN_POINT('Origin',(0.22,0.,0.));
#6323=CARTESIAN_POINT('',(-0.22,-6.93889390390723E-18,-2.69422295812418E-17));
#6324=CARTESIAN_POINT('Origin',(0.,0.,0.));
#6325=CARTESIAN_POINT('Origin',(0.,-0.02,0.));
#6326=CARTESIAN_POINT('',(-0.1954,-0.0492,2.39295984553393E-17));
#6327=CARTESIAN_POINT('Origin',(0.,-0.0492,0.));
#6328=CARTESIAN_POINT('',(-0.21,-0.02,-2.57175827820944E-17));
#6329=CARTESIAN_POINT('Origin',(0.,-0.8,0.));
#6330=CARTESIAN_POINT('',(-0.1954,-1.5646,2.39295984553393E-17));
#6331=CARTESIAN_POINT('Origin',(0.,-1.5646,0.));
#6332=CARTESIAN_POINT('',(-0.1954,-0.8,-2.39295984553393E-17));
#6333=CARTESIAN_POINT('Origin',(0.,-1.58,0.));
#6334=CARTESIAN_POINT('',(-0.16,-1.6,-1.95943487863577E-17));
#6335=CARTESIAN_POINT('Origin',(0.,-1.6,0.));
#6336=CARTESIAN_POINT('',(-0.18,-1.58,-2.20436423846524E-17));
#6337=CARTESIAN_POINT('Origin',(0.,-1.6,0.));
#6338=CARTESIAN_POINT('Origin',(0.0866025403784439,-0.4,-0.15));
#6339=CARTESIAN_POINT('',(0.173205080756888,-0.4,0.));
#6340=CARTESIAN_POINT('',(0.0866025403784439,-0.4,-0.15));
#6341=CARTESIAN_POINT('',(0.173205080756888,-0.4,0.));
#6342=CARTESIAN_POINT('',(0.0866025403784439,-0.64,-0.15));
#6343=CARTESIAN_POINT('',(0.0866025403784439,-0.4,-0.15));
#6344=CARTESIAN_POINT('',(0.173205080756888,-0.64,0.));
#6345=CARTESIAN_POINT('',(0.173205080756888,-0.64,0.));
#6346=CARTESIAN_POINT('',(0.173205080756888,-0.4,0.));
#6347=CARTESIAN_POINT('Origin',(-0.0866025403784438,-0.4,-0.15));
#6348=CARTESIAN_POINT('',(-0.0866025403784438,-0.4,-0.15));
#6349=CARTESIAN_POINT('',(0.0866025403784439,-0.4,-0.15));
#6350=CARTESIAN_POINT('',(-0.0866025403784438,-0.64,-0.15));
#6351=CARTESIAN_POINT('',(-0.0866025403784438,-0.4,-0.15));
#6352=CARTESIAN_POINT('',(0.0866025403784439,-0.64,-0.15));
#6353=CARTESIAN_POINT('Origin',(-0.173205080756888,-0.4,-2.77555756156289E-17));
#6354=CARTESIAN_POINT('',(-0.173205080756888,-0.4,-2.12115047744981E-17));
#6355=CARTESIAN_POINT('',(-0.0866025403784438,-0.4,-0.15));
#6356=CARTESIAN_POINT('',(-0.173205080756888,-0.64,-2.77555756156289E-17));
#6357=CARTESIAN_POINT('',(-0.173205080756888,-0.4,-2.12115047744981E-17));
#6358=CARTESIAN_POINT('',(-0.0866025403784438,-0.64,-0.15));
#6359=CARTESIAN_POINT('Origin',(-0.0866025403784439,-0.4,0.15));
#6360=CARTESIAN_POINT('',(-0.0866025403784439,-0.4,0.15));
#6361=CARTESIAN_POINT('',(-0.173205080756888,-0.4,-2.12115047744981E-17));
#6362=CARTESIAN_POINT('',(-0.0866025403784439,-0.64,0.15));
#6363=CARTESIAN_POINT('',(-0.0866025403784439,-0.4,0.15));
#6364=CARTESIAN_POINT('',(-0.173205080756888,-0.64,-2.12115047744981E-17));
#6365=CARTESIAN_POINT('Origin',(0.0866025403784439,-0.4,0.15));
#6366=CARTESIAN_POINT('',(0.0866025403784439,-0.4,0.15));
#6367=CARTESIAN_POINT('',(-0.0866025403784439,-0.4,0.15));
#6368=CARTESIAN_POINT('',(0.0866025403784439,-0.64,0.15));
#6369=CARTESIAN_POINT('',(0.0866025403784439,-0.4,0.15));
#6370=CARTESIAN_POINT('',(-0.0866025403784439,-0.64,0.15));
#6371=CARTESIAN_POINT('Origin',(0.173205080756888,-0.4,0.));
#6372=CARTESIAN_POINT('',(0.0866025403784439,-0.4,0.15));
#6373=CARTESIAN_POINT('',(0.0866025403784439,-0.64,0.15));
#6374=CARTESIAN_POINT('Origin',(0.,-0.4,-2.77555756156289E-17));
#6375=CARTESIAN_POINT('Origin',(0.,-0.64,-2.77555756156289E-17));
#6715=UNCERTAINTY_MEASURE_WITH_UNIT(LENGTH_MEASURE(0.001),#6744,
'DISTANCE_ACCURACY_VALUE',
'Maximum model space distance between geometric entities at asserted c
onnectivities');
#6722=UNCERTAINTY_MEASURE_WITH_UNIT(LENGTH_MEASURE(0.001),#6744,
'DISTANCE_ACCURACY_VALUE',
'Maximum model space distance between geometric entities at asserted c
onnectivities');
#6736=(
GEOMETRIC_REPRESENTATION_CONTEXT(3)
GLOBAL_UNCERTAINTY_ASSIGNED_CONTEXT((#6715))
GLOBAL_UNIT_ASSIGNED_CONTEXT((#6744,#6746,#6747))
REPRESENTATION_CONTEXT('','3D')
);
#6743=(
GEOMETRIC_REPRESENTATION_CONTEXT(3)
GLOBAL_UNCERTAINTY_ASSIGNED_CONTEXT((#6722))
GLOBAL_UNIT_ASSIGNED_CONTEXT((#6744,#6746,#6747))
REPRESENTATION_CONTEXT('','3D')
);
#6744=(
LENGTH_UNIT()
NAMED_UNIT(*)
SI_UNIT(.CENTI.,.METRE.)
);
#6746=(
NAMED_UNIT(*)
PLANE_ANGLE_UNIT()
SI_UNIT($,.RADIAN.)
);
#6747=(
NAMED_UNIT(*)
SI_UNIT($,.STERADIAN.)
SOLID_ANGLE_UNIT()
);
#6761=SHAPE_DEFINITION_REPRESENTATION(#6781,#6850);
#6781=PRODUCT_DEFINITION_SHAPE('',$,#6871);
#6850=SHAPE_REPRESENTATION('',(#4209),#6736);
#6857=PRODUCT_DEFINITION_CONTEXT('part definition',#6919,'design');
#6871=PRODUCT_DEFINITION('Cap Screw - M4x16','Cap Screw - M4x16',#6891,
#6857);
#6891=PRODUCT_DEFINITION_FORMATION('',$,#6934);
#6919=APPLICATION_CONTEXT(
'Core Data for Automotive Mechanical Design Process');
#6920=PRODUCT_CONTEXT('part definition',#6919,'mechanical');
#6934=PRODUCT('Cap Screw - M4x16','Cap Screw - M4x16',
'Cap Screw - M4x16',(#6920));
#7004=COLOUR_RGB('Black',0.12,0.14,0.17);
#7005=FILL_AREA_STYLE_COLOUR('',#7004);
#7006=FILL_AREA_STYLE('',(#7005));
#7007=SURFACE_STYLE_FILL_AREA(#7006);
#7008=SURFACE_SIDE_STYLE('',(#7007));
#7009=SURFACE_STYLE_USAGE(.BOTH.,#7008);
#7010=PRESENTATION_STYLE_ASSIGNMENT((#7009));
ENDSEC;
END-ISO-10303-21;
